ISO-10303-21;
HEADER;
/* Generated by software containing ST-Developer
 * from STEP Tools, Inc. (www.steptools.com) 
 */

FILE_DESCRIPTION(
/* description */ ('Ratchet and pawl hand winch drum'),
/* implementation_level */ '2;1');

FILE_NAME(
/* name */ 'Cap Screw - M5x20.step',
/* time_stamp */ '2026-10-27T12:42:58-07:00',
/* author */ (''),
/* organization */ (''),
/* preprocessor_version */ 'ST-DEVELOPER v20.2',
/* originating_system */ 'Autodesk Translation Framework v15.17.0.0',
/* authorisation */ '');

FILE_SCHEMA (('AUTOMOTIVE_DESIGN { 1 0 10303 214 3 1 1 }'));
ENDSEC;

DATA;
#10=MECHANICAL_DESIGN_GEOMETRIC_PRESENTATION_REPRESENTATION('',(#422),#11801);
#19=CONICAL_SURFACE('',#7263,0.4,0.785398163397448);
#20=CONICAL_SURFACE('',#7267,0.41,0.785398163397448);
#21=CONICAL_SURFACE('',#7271,0.26,0.463647609000806);
#22=CONICAL_SURFACE('',#7275,0.225,0.785398163397448);
#25=ORIENTED_CLOSED_SHELL('',*,#6302,.F.);
#28=BREP_WITH_VOIDS('Body1',#6301,(#25));
#353=SHAPE_REPRESENTATION_RELATIONSHIP('SRR','None',#11981,#387);
#387=ADVANCED_BREP_SHAPE_REPRESENTATION('',(#28),#11798);
#422=STYLED_ITEM('',(#12220),#28);
#598=FACE_BOUND('',#1675,.T.);
#824=PLANE('',#7261);
#825=PLANE('',#7269);
#826=PLANE('',#7277);
#827=PLANE('',#7278);
#828=PLANE('',#7279);
#829=PLANE('',#7280);
#830=PLANE('',#7281);
#831=PLANE('',#7282);
#832=PLANE('',#7283);
#833=PLANE('',#7284);
#834=PLANE('',#7285);
#1172=FACE_OUTER_BOUND('',#1670,.T.);
#1173=FACE_OUTER_BOUND('',#1671,.T.);
#1174=FACE_OUTER_BOUND('',#1672,.T.);
#1175=FACE_OUTER_BOUND('',#1673,.T.);
#1176=FACE_OUTER_BOUND('',#1674,.T.);
#1177=FACE_OUTER_BOUND('',#1676,.T.);
#1178=FACE_OUTER_BOUND('',#1677,.T.);
#1179=FACE_OUTER_BOUND('',#1678,.T.);
#1180=FACE_OUTER_BOUND('',#1679,.T.);
#1181=FACE_OUTER_BOUND('',#1680,.T.);
#1182=FACE_OUTER_BOUND('',#1681,.T.);
#1183=FACE_OUTER_BOUND('',#1682,.T.);
#1184=FACE_OUTER_BOUND('',#1683,.T.);
#1185=FACE_OUTER_BOUND('',#1684,.T.);
#1186=FACE_OUTER_BOUND('',#1685,.T.);
#1187=FACE_OUTER_BOUND('',#1686,.T.);
#1188=FACE_OUTER_BOUND('',#1687,.T.);
#1670=EDGE_LOOP('',(#5713));
#1671=EDGE_LOOP('',(#5714,#5715,#5716,#5717));
#1672=EDGE_LOOP('',(#5718,#5719,#5720,#5721));
#1673=EDGE_LOOP('',(#5722,#5723,#5724,#5725));
#1674=EDGE_LOOP('',(#5726));
#1675=EDGE_LOOP('',(#5727));
#1676=EDGE_LOOP('',(#5728,#5729,#5730,#5731));
#1677=EDGE_LOOP('',(#5732,#5733,#5734,#5735));
#1678=EDGE_LOOP('',(#5736,#5737,#5738,#5739));
#1679=EDGE_LOOP('',(#5740));
#1680=EDGE_LOOP('',(#5741,#5742,#5743,#5744));
#1681=EDGE_LOOP('',(#5745,#5746,#5747,#5748));
#1682=EDGE_LOOP('',(#5749,#5750,#5751,#5752));
#1683=EDGE_LOOP('',(#5753,#5754,#5755,#5756));
#1684=EDGE_LOOP('',(#5757,#5758,#5759,#5760));
#1685=EDGE_LOOP('',(#5761,#5762,#5763,#5764));
#1686=EDGE_LOOP('',(#5765,#5766,#5767,#5768,#5769,#5770));
#1687=EDGE_LOOP('',(#5771,#5772,#5773,#5774,#5775,#5776));
#2173=LINE('',#11566,#2684);
#2174=LINE('',#11570,#2685);
#2175=LINE('',#11574,#2686);
#2176=LINE('',#11581,#2687);
#2177=LINE('',#11585,#2688);
#2178=LINE('',#11589,#2689);
#2179=LINE('',#11594,#2690);
#2180=LINE('',#11596,#2691);
#2181=LINE('',#11598,#2692);
#2182=LINE('',#11599,#2693);
#2183=LINE('',#11602,#2694);
#2184=LINE('',#11604,#2695);
#2185=LINE('',#11605,#2696);
#2186=LINE('',#11608,#2697);
#2187=LINE('',#11610,#2698);
#2188=LINE('',#11611,#2699);
#2189=LINE('',#11614,#2700);
#2190=LINE('',#11616,#2701);
#2191=LINE('',#11617,#2702);
#2192=LINE('',#11620,#2703);
#2193=LINE('',#11622,#2704);
#2194=LINE('',#11623,#2705);
#2195=LINE('',#11625,#2706);
#2196=LINE('',#11626,#2707);
#2684=VECTOR('',#9006,0.4);
#2685=VECTOR('',#9011,0.425);
#2686=VECTOR('',#9016,0.41);
#2687=VECTOR('',#9025,0.26);
#2688=VECTOR('',#9030,0.25);
#2689=VECTOR('',#9035,0.225);
#2690=VECTOR('',#9040,1.);
#2691=VECTOR('',#9041,1.);
#2692=VECTOR('',#9042,1.);
#2693=VECTOR('',#9043,1.);
#2694=VECTOR('',#9046,1.);
#2695=VECTOR('',#9047,1.);
#2696=VECTOR('',#9048,1.);
#2697=VECTOR('',#9051,1.);
#2698=VECTOR('',#9052,1.);
#2699=VECTOR('',#9053,1.);
#2700=VECTOR('',#9056,1.);
#2701=VECTOR('',#9057,1.);
#2702=VECTOR('',#9058,1.);
#2703=VECTOR('',#9061,1.);
#2704=VECTOR('',#9062,1.);
#2705=VECTOR('',#9063,1.);
#2706=VECTOR('',#9066,1.);
#2707=VECTOR('',#9067,1.);
#2930=CIRCLE('',#7262,0.375);
#2931=CIRCLE('',#7264,0.425);
#2932=CIRCLE('',#7266,0.425);
#2933=CIRCLE('',#7268,0.395);
#2934=CIRCLE('',#7270,0.27);
#2935=CIRCLE('',#7272,0.24505);
#2936=CIRCLE('',#7274,0.24505);
#2937=CIRCLE('',#7276,0.2);
#3437=VERTEX_POINT('',#11561);
#3438=VERTEX_POINT('',#11564);
#3439=VERTEX_POINT('',#11568);
#3440=VERTEX_POINT('',#11572);
#3441=VERTEX_POINT('',#11576);
#3442=VERTEX_POINT('',#11579);
#3443=VERTEX_POINT('',#11583);
#3444=VERTEX_POINT('',#11587);
#3445=VERTEX_POINT('',#11592);
#3446=VERTEX_POINT('',#11593);
#3447=VERTEX_POINT('',#11595);
#3448=VERTEX_POINT('',#11597);
#3449=VERTEX_POINT('',#11601);
#3450=VERTEX_POINT('',#11603);
#3451=VERTEX_POINT('',#11607);
#3452=VERTEX_POINT('',#11609);
#3453=VERTEX_POINT('',#11613);
#3454=VERTEX_POINT('',#11615);
#3455=VERTEX_POINT('',#11619);
#3456=VERTEX_POINT('',#11621);
#4200=EDGE_CURVE('',#3437,#3437,#2930,.T.);
#4201=EDGE_CURVE('',#3438,#3438,#2931,.T.);
#4202=EDGE_CURVE('',#3438,#3437,#2173,.T.);
#4203=EDGE_CURVE('',#3439,#3439,#2932,.T.);
#4204=EDGE_CURVE('',#3439,#3438,#2174,.T.);
#4205=EDGE_CURVE('',#3440,#3440,#2933,.T.);
#4206=EDGE_CURVE('',#3440,#3439,#2175,.T.);
#4207=EDGE_CURVE('',#3441,#3441,#2934,.T.);
#4208=EDGE_CURVE('',#3442,#3442,#2935,.F.);
#4209=EDGE_CURVE('',#3442,#3441,#2176,.T.);
#4210=EDGE_CURVE('',#3443,#3443,#2936,.F.);
#4211=EDGE_CURVE('',#3443,#3442,#2177,.T.);
#4212=EDGE_CURVE('',#3444,#3444,#2937,.T.);
#4213=EDGE_CURVE('',#3444,#3443,#2178,.T.);
#4214=EDGE_CURVE('',#3445,#3446,#2179,.T.);
#4215=EDGE_CURVE('',#3446,#3447,#2180,.T.);
#4216=EDGE_CURVE('',#3447,#3448,#2181,.T.);
#4217=EDGE_CURVE('',#3445,#3448,#2182,.T.);
#4218=EDGE_CURVE('',#3446,#3449,#2183,.T.);
#4219=EDGE_CURVE('',#3449,#3450,#2184,.T.);
#4220=EDGE_CURVE('',#3450,#3447,#2185,.T.);
#4221=EDGE_CURVE('',#3449,#3451,#2186,.T.);
#4222=EDGE_CURVE('',#3451,#3452,#2187,.T.);
#4223=EDGE_CURVE('',#3452,#3450,#2188,.T.);
#4224=EDGE_CURVE('',#3451,#3453,#2189,.T.);
#4225=EDGE_CURVE('',#3453,#3454,#2190,.T.);
#4226=EDGE_CURVE('',#3454,#3452,#2191,.T.);
#4227=EDGE_CURVE('',#3453,#3455,#2192,.T.);
#4228=EDGE_CURVE('',#3455,#3456,#2193,.T.);
#4229=EDGE_CURVE('',#3456,#3454,#2194,.T.);
#4230=EDGE_CURVE('',#3455,#3445,#2195,.T.);
#4231=EDGE_CURVE('',#3448,#3456,#2196,.T.);
#5713=ORIENTED_EDGE('',*,*,#4200,.F.);
#5714=ORIENTED_EDGE('',*,*,#4201,.F.);
#5715=ORIENTED_EDGE('',*,*,#4202,.T.);
#5716=ORIENTED_EDGE('',*,*,#4200,.T.);
#5717=ORIENTED_EDGE('',*,*,#4202,.F.);
#5718=ORIENTED_EDGE('',*,*,#4203,.F.);
#5719=ORIENTED_EDGE('',*,*,#4204,.T.);
#5720=ORIENTED_EDGE('',*,*,#4201,.T.);
#5721=ORIENTED_EDGE('',*,*,#4204,.F.);
#5722=ORIENTED_EDGE('',*,*,#4205,.F.);
#5723=ORIENTED_EDGE('',*,*,#4206,.T.);
#5724=ORIENTED_EDGE('',*,*,#4203,.T.);
#5725=ORIENTED_EDGE('',*,*,#4206,.F.);
#5726=ORIENTED_EDGE('',*,*,#4205,.T.);
#5727=ORIENTED_EDGE('',*,*,#4207,.F.);
#5728=ORIENTED_EDGE('',*,*,#4208,.F.);
#5729=ORIENTED_EDGE('',*,*,#4209,.T.);
#5730=ORIENTED_EDGE('',*,*,#4207,.T.);
#5731=ORIENTED_EDGE('',*,*,#4209,.F.);
#5732=ORIENTED_EDGE('',*,*,#4210,.F.);
#5733=ORIENTED_EDGE('',*,*,#4211,.T.);
#5734=ORIENTED_EDGE('',*,*,#4208,.T.);
#5735=ORIENTED_EDGE('',*,*,#4211,.F.);
#5736=ORIENTED_EDGE('',*,*,#4212,.F.);
#5737=ORIENTED_EDGE('',*,*,#4213,.T.);
#5738=ORIENTED_EDGE('',*,*,#4210,.T.);
#5739=ORIENTED_EDGE('',*,*,#4213,.F.);
#5740=ORIENTED_EDGE('',*,*,#4212,.T.);
#5741=ORIENTED_EDGE('',*,*,#4214,.T.);
#5742=ORIENTED_EDGE('',*,*,#4215,.T.);
#5743=ORIENTED_EDGE('',*,*,#4216,.T.);
#5744=ORIENTED_EDGE('',*,*,#4217,.F.);
#5745=ORIENTED_EDGE('',*,*,#4218,.T.);
#5746=ORIENTED_EDGE('',*,*,#4219,.T.);
#5747=ORIENTED_EDGE('',*,*,#4220,.T.);
#5748=ORIENTED_EDGE('',*,*,#4215,.F.);
#5749=ORIENTED_EDGE('',*,*,#4221,.T.);
#5750=ORIENTED_EDGE('',*,*,#4222,.T.);
#5751=ORIENTED_EDGE('',*,*,#4223,.T.);
#5752=ORIENTED_EDGE('',*,*,#4219,.F.);
#5753=ORIENTED_EDGE('',*,*,#4224,.T.);
#5754=ORIENTED_EDGE('',*,*,#4225,.T.);
#5755=ORIENTED_EDGE('',*,*,#4226,.T.);
#5756=ORIENTED_EDGE('',*,*,#4222,.F.);
#5757=ORIENTED_EDGE('',*,*,#4227,.T.);
#5758=ORIENTED_EDGE('',*,*,#4228,.T.);
#5759=ORIENTED_EDGE('',*,*,#4229,.T.);
#5760=ORIENTED_EDGE('',*,*,#4225,.F.);
#5761=ORIENTED_EDGE('',*,*,#4230,.T.);
#5762=ORIENTED_EDGE('',*,*,#4217,.T.);
#5763=ORIENTED_EDGE('',*,*,#4231,.T.);
#5764=ORIENTED_EDGE('',*,*,#4228,.F.);
#5765=ORIENTED_EDGE('',*,*,#4230,.F.);
#5766=ORIENTED_EDGE('',*,*,#4227,.F.);
#5767=ORIENTED_EDGE('',*,*,#4224,.F.);
#5768=ORIENTED_EDGE('',*,*,#4221,.F.);
#5769=ORIENTED_EDGE('',*,*,#4218,.F.);
#5770=ORIENTED_EDGE('',*,*,#4214,.F.);
#5771=ORIENTED_EDGE('',*,*,#4231,.F.);
#5772=ORIENTED_EDGE('',*,*,#4216,.F.);
#5773=ORIENTED_EDGE('',*,*,#4220,.F.);
#5774=ORIENTED_EDGE('',*,*,#4223,.F.);
#5775=ORIENTED_EDGE('',*,*,#4226,.F.);
#5776=ORIENTED_EDGE('',*,*,#4229,.F.);
#5906=CYLINDRICAL_SURFACE('',#7265,0.425);
#5907=CYLINDRICAL_SURFACE('',#7273,0.24505);
#6242=ADVANCED_FACE('',(#1172),#824,.T.);
#6243=ADVANCED_FACE('',(#1173),#19,.T.);
#6244=ADVANCED_FACE('',(#1174),#5906,.T.);
#6245=ADVANCED_FACE('',(#1175),#20,.T.);
#6246=ADVANCED_FACE('',(#1176,#598),#825,.T.);
#6247=ADVANCED_FACE('',(#1177),#21,.T.);
#6248=ADVANCED_FACE('',(#1178),#5907,.T.);
#6249=ADVANCED_FACE('',(#1179),#22,.T.);
#6250=ADVANCED_FACE('',(#1180),#826,.T.);
#6251=ADVANCED_FACE('',(#1181),#827,.F.);
#6252=ADVANCED_FACE('',(#1182),#828,.F.);
#6253=ADVANCED_FACE('',(#1183),#829,.F.);
#6254=ADVANCED_FACE('',(#1184),#830,.F.);
#6255=ADVANCED_FACE('',(#1185),#831,.F.);
#6256=ADVANCED_FACE('',(#1186),#832,.F.);
#6257=ADVANCED_FACE('',(#1187),#833,.F.);
#6258=ADVANCED_FACE('',(#1188),#834,.F.);
#6301=CLOSED_SHELL('',(#6242,#6243,#6244,#6245,#6246,#6247,#6248,#6249,
#6250));
#6302=CLOSED_SHELL('',(#6251,#6252,#6253,#6254,#6255,#6256,#6257,#6258));
#7260=AXIS2_PLACEMENT_3D('',#11559,#8996,#8997);
#7261=AXIS2_PLACEMENT_3D('',#11560,#8998,#8999);
#7262=AXIS2_PLACEMENT_3D('',#11562,#9000,#9001);
#7263=AXIS2_PLACEMENT_3D('',#11563,#9002,#9003);
#7264=AXIS2_PLACEMENT_3D('',#11565,#9004,#9005);
#7265=AXIS2_PLACEMENT_3D('',#11567,#9007,#9008);
#7266=AXIS2_PLACEMENT_3D('',#11569,#9009,#9010);
#7267=AXIS2_PLACEMENT_3D('',#11571,#9012,#9013);
#7268=AXIS2_PLACEMENT_3D('',#11573,#9014,#9015);
#7269=AXIS2_PLACEMENT_3D('',#11575,#9017,#9018);
#7270=AXIS2_PLACEMENT_3D('',#11577,#9019,#9020);
#7271=AXIS2_PLACEMENT_3D('',#11578,#9021,#9022);
#7272=AXIS2_PLACEMENT_3D('',#11580,#9023,#9024);
#7273=AXIS2_PLACEMENT_3D('',#11582,#9026,#9027);
#7274=AXIS2_PLACEMENT_3D('',#11584,#9028,#9029);
#7275=AXIS2_PLACEMENT_3D('',#11586,#9031,#9032);
#7276=AXIS2_PLACEMENT_3D('',#11588,#9033,#9034);
#7277=AXIS2_PLACEMENT_3D('',#11590,#9036,#9037);
#7278=AXIS2_PLACEMENT_3D('',#11591,#9038,#9039);
#7279=AXIS2_PLACEMENT_3D('',#11600,#9044,#9045);
#7280=AXIS2_PLACEMENT_3D('',#11606,#9049,#9050);
#7281=AXIS2_PLACEMENT_3D('',#11612,#9054,#9055);
#7282=AXIS2_PLACEMENT_3D('',#11618,#9059,#9060);
#7283=AXIS2_PLACEMENT_3D('',#11624,#9064,#9065);
#7284=AXIS2_PLACEMENT_3D('',#11627,#9068,#9069);
#7285=AXIS2_PLACEMENT_3D('',#11628,#9070,#9071);
#8996=DIRECTION('axis',(0.,0.,1.));
#8997=DIRECTION('refdir',(1.,0.,0.));
#8998=DIRECTION('center_axis',(0.,1.,0.));
#8999=DIRECTION('ref_axis',(0.,0.,1.));
#9000=DIRECTION('center_axis',(0.,-1.,0.));
#9001=DIRECTION('ref_axis',(1.,0.,0.));
#9002=DIRECTION('center_axis',(0.,-1.,0.));
#9003=DIRECTION('ref_axis',(1.,0.,0.));
#9004=DIRECTION('center_axis',(0.,-1.,0.));
#9005=DIRECTION('ref_axis',(1.,0.,0.));
#9006=DIRECTION('',(0.707106781186548,0.707106781186547,8.65956056235493E-17));
#9007=DIRECTION('center_axis',(0.,-1.,0.));
#9008=DIRECTION('ref_axis',(1.,0.,0.));
#9009=DIRECTION('center_axis',(0.,-1.,0.));
#9010=DIRECTION('ref_axis',(1.,0.,0.));
#9011=DIRECTION('',(0.,1.,0.));
#9012=DIRECTION('center_axis',(0.,1.,0.));
#9013=DIRECTION('ref_axis',(1.,0.,0.));
#9014=DIRECTION('center_axis',(0.,-1.,0.));
#9015=DIRECTION('ref_axis',(1.,0.,0.));
#9016=DIRECTION('',(-0.707106781186547,0.707106781186548,-8.65956056235493E-17));
#9017=DIRECTION('center_axis',(0.,-1.,0.));
#9018=DIRECTION('ref_axis',(0.,0.,-1.));
#9019=DIRECTION('center_axis',(0.,-1.,0.));
#9020=DIRECTION('ref_axis',(1.,0.,0.));
#9021=DIRECTION('center_axis',(0.,1.,0.));
#9022=DIRECTION('ref_axis',(1.,0.,0.));
#9023=DIRECTION('center_axis',(0.,1.,0.));
#9024=DIRECTION('ref_axis',(1.,0.,0.));
#9025=DIRECTION('',(-0.447213595499958,0.894427190999916,-5.47678698264203E-17));
#9026=DIRECTION('center_axis',(0.,-1.,0.));
#9027=DIRECTION('ref_axis',(1.,0.,0.));
#9028=DIRECTION('center_axis',(0.,1.,0.));
#9029=DIRECTION('ref_axis',(1.,0.,0.));
#9030=DIRECTION('',(0.,1.,0.));
#9031=DIRECTION('center_axis',(0.,1.,0.));
#9032=DIRECTION('ref_axis',(1.,0.,0.));
#9033=DIRECTION('center_axis',(0.,-1.,0.));
#9034=DIRECTION('ref_axis',(1.,0.,0.));
#9035=DIRECTION('',(-0.707106781186547,0.707106781186548,-8.65956056235493E-17));
#9036=DIRECTION('center_axis',(0.,-1.,0.));
#9037=DIRECTION('ref_axis',(0.,0.,-1.));
#9038=DIRECTION('center_axis',(0.866025403784439,0.,-0.5));
#9039=DIRECTION('ref_axis',(0.5,0.,0.866025403784439));
#9040=DIRECTION('',(-0.5,0.,-0.866025403784439));
#9041=DIRECTION('',(0.,-1.,0.));
#9042=DIRECTION('',(0.5,0.,0.866025403784439));
#9043=DIRECTION('',(0.,-1.,0.));
#9044=DIRECTION('center_axis',(1.20185167898973E-16,0.,-1.));
#9045=DIRECTION('ref_axis',(1.,0.,1.20185167898973E-16));
#9046=DIRECTION('',(-1.,0.,-1.20185167898973E-16));
#9047=DIRECTION('',(0.,-1.,0.));
#9048=DIRECTION('',(1.,0.,1.20185167898973E-16));
#9049=DIRECTION('center_axis',(-0.866025403784439,0.,-0.5));
#9050=DIRECTION('ref_axis',(0.5,0.,-0.866025403784439));
#9051=DIRECTION('',(-0.5,0.,0.866025403784439));
#9052=DIRECTION('',(0.,-1.,0.));
#9053=DIRECTION('',(0.5,0.,-0.866025403784439));
#9054=DIRECTION('center_axis',(-0.866025403784439,0.,0.5));
#9055=DIRECTION('ref_axis',(-0.5,0.,-0.866025403784439));
#9056=DIRECTION('',(0.5,0.,0.866025403784439));
#9057=DIRECTION('',(0.,-1.,0.));
#9058=DIRECTION('',(-0.5,0.,-0.866025403784439));
#9059=DIRECTION('center_axis',(-2.40370335797945E-16,0.,1.));
#9060=DIRECTION('ref_axis',(-1.,0.,-2.40370335797945E-16));
#9061=DIRECTION('',(1.,0.,2.40370335797945E-16));
#9062=DIRECTION('',(0.,-1.,0.));
#9063=DIRECTION('',(-1.,0.,-2.40370335797945E-16));
#9064=DIRECTION('center_axis',(0.866025403784439,0.,0.5));
#9065=DIRECTION('ref_axis',(-0.5,0.,0.866025403784439));
#9066=DIRECTION('',(0.5,0.,-0.866025403784439));
#9067=DIRECTION('',(-0.5,0.,0.866025403784439));
#9068=DIRECTION('center_axis',(0.,1.,0.));
#9069=DIRECTION('ref_axis',(1.,0.,0.));
#9070=DIRECTION('center_axis',(0.,-1.,0.));
#9071=DIRECTION('ref_axis',(0.,0.,-1.));
#11559=CARTESIAN_POINT('',(0.,0.,0.));
#11560=CARTESIAN_POINT('Origin',(0.375,0.5,0.));
#11561=CARTESIAN_POINT('',(-0.375,0.5,-4.59242549680257E-17));
#11562=CARTESIAN_POINT('Origin',(0.,0.5,0.));
#11563=CARTESIAN_POINT('Origin',(0.,0.475,0.));
#11564=CARTESIAN_POINT('',(-0.425,0.45,-5.20474889637625E-17));
#11565=CARTESIAN_POINT('Origin',(0.,0.45,0.));
#11566=CARTESIAN_POINT('',(-0.4,0.475,-4.89858719658941E-17));
#11567=CARTESIAN_POINT('Origin',(0.,0.24,0.));
#11568=CARTESIAN_POINT('',(-0.425,0.0299999999999998,-5.20474889637625E-17));
#11569=CARTESIAN_POINT('Origin',(0.,0.0299999999999998,0.));
#11570=CARTESIAN_POINT('',(-0.425,0.24,-5.20474889637625E-17));
#11571=CARTESIAN_POINT('Origin',(0.,0.0150000000000001,0.));
#11572=CARTESIAN_POINT('',(-0.395,4.85722573273506E-17,-4.83735485663204E-17));
#11573=CARTESIAN_POINT('Origin',(0.,0.,0.));
#11574=CARTESIAN_POINT('',(-0.41,0.0150000000000001,-5.02105187650415E-17));
#11575=CARTESIAN_POINT('Origin',(0.27,0.,0.));
#11576=CARTESIAN_POINT('',(-0.27,0.,-3.30654635769785E-17));
#11577=CARTESIAN_POINT('Origin',(0.,0.,0.));
#11578=CARTESIAN_POINT('Origin',(0.,-0.02,0.));
#11579=CARTESIAN_POINT('',(-0.24505,-0.0498999999999999,3.00099698131059E-17));
#11580=CARTESIAN_POINT('Origin',(0.,-0.0498999999999999,0.));
#11581=CARTESIAN_POINT('',(-0.26,-0.02,-3.18408167778312E-17));
#11582=CARTESIAN_POINT('Origin',(0.,-0.995,0.));
#11583=CARTESIAN_POINT('',(-0.24505,-1.95495,3.00099698131059E-17));
#11584=CARTESIAN_POINT('Origin',(0.,-1.95495,0.));
#11585=CARTESIAN_POINT('',(-0.24505,-0.995,-3.00099698131059E-17));
#11586=CARTESIAN_POINT('Origin',(0.,-1.975,0.));
#11587=CARTESIAN_POINT('',(-0.2,-2.,-2.44929359829471E-17));
#11588=CARTESIAN_POINT('Origin',(0.,-2.,0.));
#11589=CARTESIAN_POINT('',(-0.225,-1.975,-2.75545529808154E-17));
#11590=CARTESIAN_POINT('Origin',(0.,-2.,0.));
#11591=CARTESIAN_POINT('Origin',(0.115470053837925,-0.5,-0.2));
#11592=CARTESIAN_POINT('',(0.23094010767585,-0.5,0.));
#11593=CARTESIAN_POINT('',(0.115470053837925,-0.5,-0.2));
#11594=CARTESIAN_POINT('',(0.23094010767585,-0.5,0.));
#11595=CARTESIAN_POINT('',(0.115470053837925,-0.8,-0.2));
#11596=CARTESIAN_POINT('',(0.115470053837925,-0.5,-0.2));
#11597=CARTESIAN_POINT('',(0.23094010767585,-0.8,0.));
#11598=CARTESIAN_POINT('',(0.23094010767585,-0.8,0.));
#11599=CARTESIAN_POINT('',(0.23094010767585,-0.5,0.));
#11600=CARTESIAN_POINT('Origin',(-0.115470053837925,-0.5,-0.2));
#11601=CARTESIAN_POINT('',(-0.115470053837925,-0.5,-0.2));
#11602=CARTESIAN_POINT('',(0.115470053837925,-0.5,-0.2));
#11603=CARTESIAN_POINT('',(-0.115470053837925,-0.8,-0.2));
#11604=CARTESIAN_POINT('',(-0.115470053837925,-0.5,-0.2));
#11605=CARTESIAN_POINT('',(0.115470053837925,-0.8,-0.2));
#11606=CARTESIAN_POINT('Origin',(-0.23094010767585,-0.5,-2.77555756156289E-17));
#11607=CARTESIAN_POINT('',(-0.23094010767585,-0.5,-2.82820063659975E-17));
#11608=CARTESIAN_POINT('',(-0.115470053837925,-0.5,-0.2));
#11609=CARTESIAN_POINT('',(-0.23094010767585,-0.8,-2.77555756156289E-17));
#11610=CARTESIAN_POINT('',(-0.23094010767585,-0.5,-2.82820063659975E-17));
#11611=CARTESIAN_POINT('',(-0.115470053837925,-0.8,-0.2));
#11612=CARTESIAN_POINT('Origin',(-0.115470053837925,-0.5,0.2));
#11613=CARTESIAN_POINT('',(-0.115470053837925,-0.5,0.2));
#11614=CARTESIAN_POINT('',(-0.23094010767585,-0.5,-2.82820063659975E-17));
#11615=CARTESIAN_POINT('',(-0.115470053837925,-0.8,0.2));
#11616=CARTESIAN_POINT('',(-0.115470053837925,-0.5,0.2));
#11617=CARTESIAN_POINT('',(-0.23094010767585,-0.8,-2.82820063659975E-17));
#11618=CARTESIAN_POINT('Origin',(0.115470053837925,-0.5,0.2));
#11619=CARTESIAN_POINT('',(0.115470053837925,-0.5,0.2));
#11620=CARTESIAN_POINT('',(-0.115470053837925,-0.5,0.2));
#11621=CARTESIAN_POINT('',(0.115470053837925,-0.8,0.2));
#11622=CARTESIAN_POINT('',(0.115470053837925,-0.5,0.2));
#11623=CARTESIAN_POINT('',(-0.115470053837925,-0.8,0.2));
#11624=CARTESIAN_POINT('Origin',(0.23094010767585,-0.5,0.));
#11625=CARTESIAN_POINT('',(0.115470053837925,-0.5,0.2));
#11626=CARTESIAN_POINT('',(0.115470053837925,-0.8,0.2));
#11627=CARTESIAN_POINT('Origin',(0.,-0.5,0.));
#11628=CARTESIAN_POINT('Origin',(0.,-0.8,0.));
#11758=UNCERTAINTY_MEASURE_WITH_UNIT(LENGTH_MEASURE(0.001),#11802,
'DISTANCE_ACCURACY_VALUE',
'Maximum model space distance between geometric entities at asserted c
onnectivities');
#11761=UNCERTAINTY_MEASURE_WITH_UNIT(LENGTH_MEASURE(0.001),#11802,
'DISTANCE_ACCURACY_VALUE',
'Maximum model space distance between geometric entities at asserted c
onnectivities');
#11798=(
GEOMETRIC_REPRESENTATION_CONTEXT(3)
GLOBAL_UNCERTAINTY_ASSIGNED_CONTEXT((#11758))
GLOBAL_UNIT_ASSIGNED_CONTEXT((#11802,#11804,#11805))
REPRESENTATION_CONTEXT('','3D')
);
#11801=(
GEOMETRIC_REPRESENTATION_CONTEXT(3)
GLOBAL_UNCERTAINTY_ASSIGNED_CONTEXT((#11761))
GLOBAL_UNIT_ASSIGNED_CONTEXT((#11802,#11804,#11805))
REPRESENTATION_CONTEXT('','3D')
);
#11802=(
LENGTH_UNIT()
NAMED_UNIT(*)
SI_UNIT(.CENTI.,.METRE.)
);
#11804=(
NAMED_UNIT(*)
PLANE_ANGLE_UNIT()
SI_UNIT($,.RADIAN.)
);
#11805=(
NAMED_UNIT(*)
SI_UNIT($,.STERADIAN.)
SOLID_ANGLE_UNIT()
);
#11842=SHAPE_DEFINITION_REPRESENTATION(#11883,#11981);
#11883=PRODUCT_DEFINITION_SHAPE('',$,#12021);
#11981=SHAPE_REPRESENTATION('',(#7260),#11798);
#11984=PRODUCT_DEFINITION_CONTEXT('part definition',#12103,'design');
#12021=PRODUCT_DEFINITION('Cap Screw - M5x20','Cap Screw - M5x20',#12060,
#11984);
#12060=PRODUCT_DEFINITION_FORMATION('',$,#12141);
#12103=APPLICATION_CONTEXT(
'Core Data for Automotive Mechanical Design Process');
#12104=PRODUCT_CONTEXT('part definition',#12103,'mechanical');
#12141=PRODUCT('Cap Screw - M5x20','Cap Screw - M5x20',
'Cap Screw - M5x20',(#12104));
#12214=COLOUR_RGB('Black',0.12,0.14,0.17);
#12215=FILL_AREA_STYLE_COLOUR('',#12214);
#12216=FILL_AREA_STYLE('',(#12215));
#12217=SURFACE_STYLE_FILL_AREA(#12216);
#12218=SURFACE_SIDE_STYLE('',(#12217));
#12219=SURFACE_STYLE_USAGE(.BOTH.,#12218);
#12220=PRESENTATION_STYLE_ASSIGNMENT((#12219));
ENDSEC;
END-ISO-10303-21;
